ISO-10303-21;
HEADER;
/* Generated by software containing ST-Developer
 * from STEP Tools, Inc. (www.steptools.com) 
 */

FILE_DESCRIPTION(
/* description */ (''),
/* implementation_level */ '2;1');

FILE_NAME(
/* name */ 'Blade_06.step',
/* time_stamp */ '2026-10-23T22:28:14+06:00',
/* author */ (''),
/* organization */ (''),
/* preprocessor_version */ 'ST-DEVELOPER v20.2',
/* originating_system */ 'Autodesk Translation Framework v15.15.0.0',
/* authorisation */ '');

FILE_SCHEMA (('AUTOMOTIVE_DESIGN { 1 0 10303 214 3 1 1 }'));
ENDSEC;

DATA;
#10=MECHANICAL_DESIGN_GEOMETRIC_PRESENTATION_REPRESENTATION('',(#112),#6753);
#86=SHAPE_REPRESENTATION_RELATIONSHIP('SRR','None',#6809,#99);
#99=ADVANCED_BREP_SHAPE_REPRESENTATION('',(#125),#6749);
#112=STYLED_ITEM('',(#6935),#125);
#125=MANIFOLD_SOLID_BREP('Blade_06',#3761);
#178=FACE_BOUND('',#771,.T.);
#179=FACE_BOUND('',#772,.T.);
#309=PLANE('',#4277);
#310=PLANE('',#4278);
#311=PLANE('',#4279);
#312=PLANE('',#4286);
#313=PLANE('',#4289);
#314=PLANE('',#4294);
#506=FACE_OUTER_BOUND('',#768,.T.);
#507=FACE_OUTER_BOUND('',#769,.T.);
#508=FACE_OUTER_BOUND('',#770,.T.);
#509=FACE_OUTER_BOUND('',#773,.T.);
#510=FACE_OUTER_BOUND('',#774,.T.);
#511=FACE_OUTER_BOUND('',#775,.T.);
#512=FACE_OUTER_BOUND('',#776,.T.);
#513=FACE_OUTER_BOUND('',#777,.T.);
#514=FACE_OUTER_BOUND('',#778,.T.);
#515=FACE_OUTER_BOUND('',#779,.T.);
#768=EDGE_LOOP('',(#3334,#3335,#3336,#3337));
#769=EDGE_LOOP('',(#3338,#3339,#3340,#3341));
#770=EDGE_LOOP('',(#3342,#3343,#3344,#3345));
#771=EDGE_LOOP('',(#3346));
#772=EDGE_LOOP('',(#3347));
#773=EDGE_LOOP('',(#3348,#3349,#3350,#3351));
#774=EDGE_LOOP('',(#3352));
#775=EDGE_LOOP('',(#3353,#3354,#3355,#3356));
#776=EDGE_LOOP('',(#3357));
#777=EDGE_LOOP('',(#3358,#3359,#3360,#3361));
#778=EDGE_LOOP('',(#3362,#3363,#3364,#3365));
#779=EDGE_LOOP('',(#3366,#3367,#3368,#3369));
#1000=CIRCLE('',#4280,33.8);
#1001=CIRCLE('',#4281,4.99999999999999);
#1002=CIRCLE('',#4282,1.1);
#1003=CIRCLE('',#4283,1.1);
#1004=CIRCLE('',#4285,1.1);
#1005=CIRCLE('',#4288,1.1);
#1006=CIRCLE('',#4291,4.99999999999999);
#1007=CIRCLE('',#4293,33.8);
#1278=LINE('',#6551,#1564);
#1279=LINE('',#6553,#1565);
#1280=LINE('',#6555,#1566);
#1281=LINE('',#6556,#1567);
#1282=LINE('',#6560,#1568);
#1283=LINE('',#6562,#1569);
#1284=LINE('',#6564,#1570);
#1285=LINE('',#6565,#1571);
#1286=LINE('',#6576,#1572);
#1287=LINE('',#6581,#1573);
#1564=VECTOR('',#5349,10.);
#1565=VECTOR('',#5350,10.);
#1566=VECTOR('',#5351,10.);
#1567=VECTOR('',#5352,10.);
#1568=VECTOR('',#5355,10.);
#1569=VECTOR('',#5356,10.);
#1570=VECTOR('',#5357,10.);
#1571=VECTOR('',#5358,10.);
#1572=VECTOR('',#5373,1.1);
#1573=VECTOR('',#5380,1.1);
#1897=VERTEX_POINT('',#6549);
#1898=VERTEX_POINT('',#6550);
#1899=VERTEX_POINT('',#6552);
#1900=VERTEX_POINT('',#6554);
#1901=VERTEX_POINT('',#6558);
#1902=VERTEX_POINT('',#6559);
#1903=VERTEX_POINT('',#6561);
#1904=VERTEX_POINT('',#6563);
#1905=VERTEX_POINT('',#6569);
#1906=VERTEX_POINT('',#6571);
#1907=VERTEX_POINT('',#6574);
#1908=VERTEX_POINT('',#6579);
#2384=EDGE_CURVE('',#1897,#1898,#1278,.T.);
#2385=EDGE_CURVE('',#1899,#1897,#1279,.T.);
#2386=EDGE_CURVE('',#1900,#1899,#1280,.T.);
#2387=EDGE_CURVE('',#1898,#1900,#1281,.T.);
#2388=EDGE_CURVE('',#1901,#1902,#1282,.T.);
#2389=EDGE_CURVE('',#1903,#1901,#1283,.T.);
#2390=EDGE_CURVE('',#1904,#1903,#1284,.T.);
#2391=EDGE_CURVE('',#1902,#1904,#1285,.T.);
#2392=EDGE_CURVE('',#1901,#1898,#1000,.T.);
#2393=EDGE_CURVE('',#1897,#1902,#1001,.T.);
#2394=EDGE_CURVE('',#1905,#1905,#1002,.T.);
#2395=EDGE_CURVE('',#1906,#1906,#1003,.T.);
#2396=EDGE_CURVE('',#1907,#1907,#1004,.T.);
#2397=EDGE_CURVE('',#1907,#1905,#1286,.T.);
#2398=EDGE_CURVE('',#1908,#1908,#1005,.T.);
#2399=EDGE_CURVE('',#1908,#1906,#1287,.T.);
#2400=EDGE_CURVE('',#1899,#1904,#1006,.T.);
#2401=EDGE_CURVE('',#1903,#1900,#1007,.T.);
#3334=ORIENTED_EDGE('',*,*,#2384,.F.);
#3335=ORIENTED_EDGE('',*,*,#2385,.F.);
#3336=ORIENTED_EDGE('',*,*,#2386,.F.);
#3337=ORIENTED_EDGE('',*,*,#2387,.F.);
#3338=ORIENTED_EDGE('',*,*,#2388,.F.);
#3339=ORIENTED_EDGE('',*,*,#2389,.F.);
#3340=ORIENTED_EDGE('',*,*,#2390,.F.);
#3341=ORIENTED_EDGE('',*,*,#2391,.F.);
#3342=ORIENTED_EDGE('',*,*,#2384,.T.);
#3343=ORIENTED_EDGE('',*,*,#2392,.F.);
#3344=ORIENTED_EDGE('',*,*,#2388,.T.);
#3345=ORIENTED_EDGE('',*,*,#2393,.F.);
#3346=ORIENTED_EDGE('',*,*,#2394,.T.);
#3347=ORIENTED_EDGE('',*,*,#2395,.T.);
#3348=ORIENTED_EDGE('',*,*,#2396,.F.);
#3349=ORIENTED_EDGE('',*,*,#2397,.T.);
#3350=ORIENTED_EDGE('',*,*,#2394,.F.);
#3351=ORIENTED_EDGE('',*,*,#2397,.F.);
#3352=ORIENTED_EDGE('',*,*,#2396,.T.);
#3353=ORIENTED_EDGE('',*,*,#2398,.F.);
#3354=ORIENTED_EDGE('',*,*,#2399,.T.);
#3355=ORIENTED_EDGE('',*,*,#2395,.F.);
#3356=ORIENTED_EDGE('',*,*,#2399,.F.);
#3357=ORIENTED_EDGE('',*,*,#2398,.T.);
#3358=ORIENTED_EDGE('',*,*,#2385,.T.);
#3359=ORIENTED_EDGE('',*,*,#2393,.T.);
#3360=ORIENTED_EDGE('',*,*,#2391,.T.);
#3361=ORIENTED_EDGE('',*,*,#2400,.F.);
#3362=ORIENTED_EDGE('',*,*,#2387,.T.);
#3363=ORIENTED_EDGE('',*,*,#2401,.F.);
#3364=ORIENTED_EDGE('',*,*,#2389,.T.);
#3365=ORIENTED_EDGE('',*,*,#2392,.T.);
#3366=ORIENTED_EDGE('',*,*,#2386,.T.);
#3367=ORIENTED_EDGE('',*,*,#2400,.T.);
#3368=ORIENTED_EDGE('',*,*,#2390,.T.);
#3369=ORIENTED_EDGE('',*,*,#2401,.T.);
#3523=CYLINDRICAL_SURFACE('',#4284,1.1);
#3524=CYLINDRICAL_SURFACE('',#4287,1.1);
#3525=CYLINDRICAL_SURFACE('',#4290,4.99999999999999);
#3526=CYLINDRICAL_SURFACE('',#4292,33.8);
#3712=ADVANCED_FACE('',(#506),#309,.F.);
#3713=ADVANCED_FACE('',(#507),#310,.F.);
#3714=ADVANCED_FACE('',(#508,#178,#179),#311,.F.);
#3715=ADVANCED_FACE('',(#509),#3523,.T.);
#3716=ADVANCED_FACE('',(#510),#312,.F.);
#3717=ADVANCED_FACE('',(#511),#3524,.T.);
#3718=ADVANCED_FACE('',(#512),#313,.F.);
#3719=ADVANCED_FACE('',(#513),#3525,.F.);
#3720=ADVANCED_FACE('',(#514),#3526,.T.);
#3721=ADVANCED_FACE('',(#515),#314,.T.);
#3761=CLOSED_SHELL('',(#3712,#3713,#3714,#3715,#3716,#3717,#3718,#3719,
#3720,#3721));
#4276=AXIS2_PLACEMENT_3D('',#6547,#5345,#5346);
#4277=AXIS2_PLACEMENT_3D('',#6548,#5347,#5348);
#4278=AXIS2_PLACEMENT_3D('',#6557,#5353,#5354);
#4279=AXIS2_PLACEMENT_3D('',#6566,#5359,#5360);
#4280=AXIS2_PLACEMENT_3D('',#6567,#5361,#5362);
#4281=AXIS2_PLACEMENT_3D('',#6568,#5363,#5364);
#4282=AXIS2_PLACEMENT_3D('',#6570,#5365,#5366);
#4283=AXIS2_PLACEMENT_3D('',#6572,#5367,#5368);
#4284=AXIS2_PLACEMENT_3D('',#6573,#5369,#5370);
#4285=AXIS2_PLACEMENT_3D('',#6575,#5371,#5372);
#4286=AXIS2_PLACEMENT_3D('',#6577,#5374,#5375);
#4287=AXIS2_PLACEMENT_3D('',#6578,#5376,#5377);
#4288=AXIS2_PLACEMENT_3D('',#6580,#5378,#5379);
#4289=AXIS2_PLACEMENT_3D('',#6582,#5381,#5382);
#4290=AXIS2_PLACEMENT_3D('',#6583,#5383,#5384);
#4291=AXIS2_PLACEMENT_3D('',#6584,#5385,#5386);
#4292=AXIS2_PLACEMENT_3D('',#6585,#5387,#5388);
#4293=AXIS2_PLACEMENT_3D('',#6586,#5389,#5390);
#4294=AXIS2_PLACEMENT_3D('',#6587,#5391,#5392);
#5345=DIRECTION('axis',(0.,0.,1.));
#5346=DIRECTION('refdir',(1.,0.,0.));
#5347=DIRECTION('center_axis',(1.,0.,-3.33066907387547E-16));
#5348=DIRECTION('ref_axis',(-3.33066907387547E-16,0.,-1.));
#5349=DIRECTION('',(-3.33066907387547E-16,0.,-1.));
#5350=DIRECTION('',(0.,-1.,0.));
#5351=DIRECTION('',(3.33066907387547E-16,0.,1.));
#5352=DIRECTION('',(0.,1.,0.));
#5353=DIRECTION('center_axis',(-0.707106781186548,0.,-0.707106781186547));
#5354=DIRECTION('ref_axis',(-0.707106781186547,0.,0.707106781186548));
#5355=DIRECTION('',(-0.707106781186547,0.,0.707106781186548));
#5356=DIRECTION('',(0.,-1.,0.));
#5357=DIRECTION('',(0.707106781186547,0.,-0.707106781186548));
#5358=DIRECTION('',(0.,1.,0.));
#5359=DIRECTION('center_axis',(0.,1.,0.));
#5360=DIRECTION('ref_axis',(-0.707106781186548,0.,-0.707106781186547));
#5361=DIRECTION('center_axis',(0.,1.,0.));
#5362=DIRECTION('ref_axis',(-0.707106781186548,0.,-0.707106781186547));
#5363=DIRECTION('center_axis',(0.,-1.,0.));
#5364=DIRECTION('ref_axis',(-0.707106781186548,0.,-0.707106781186547));
#5365=DIRECTION('center_axis',(0.,1.,0.));
#5366=DIRECTION('ref_axis',(-0.707106781186547,0.,-0.707106781186547));
#5367=DIRECTION('center_axis',(0.,1.,0.));
#5368=DIRECTION('ref_axis',(-0.707106781186548,0.,-0.707106781186547));
#5369=DIRECTION('center_axis',(0.,-1.,0.));
#5370=DIRECTION('ref_axis',(-0.707106781186547,0.,-0.707106781186547));
#5371=DIRECTION('center_axis',(0.,-1.,0.));
#5372=DIRECTION('ref_axis',(-0.707106781186547,0.,-0.707106781186547));
#5373=DIRECTION('',(0.,1.,0.));
#5374=DIRECTION('center_axis',(0.,1.,0.));
#5375=DIRECTION('ref_axis',(-0.707106781186548,0.,-0.707106781186547));
#5376=DIRECTION('center_axis',(0.,-1.,0.));
#5377=DIRECTION('ref_axis',(-0.707106781186548,0.,-0.707106781186547));
#5378=DIRECTION('center_axis',(0.,-1.,0.));
#5379=DIRECTION('ref_axis',(-0.707106781186548,0.,-0.707106781186547));
#5380=DIRECTION('',(0.,1.,0.));
#5381=DIRECTION('center_axis',(0.,1.,0.));
#5382=DIRECTION('ref_axis',(-0.707106781186548,0.,-0.707106781186547));
#5383=DIRECTION('center_axis',(0.,1.,0.));
#5384=DIRECTION('ref_axis',(-0.707106781186548,0.,-0.707106781186547));
#5385=DIRECTION('center_axis',(0.,-1.,0.));
#5386=DIRECTION('ref_axis',(-0.707106781186548,0.,-0.707106781186547));
#5387=DIRECTION('center_axis',(0.,1.,0.));
#5388=DIRECTION('ref_axis',(-0.707106781186548,0.,-0.707106781186547));
#5389=DIRECTION('center_axis',(0.,1.,0.));
#5390=DIRECTION('ref_axis',(-0.707106781186548,0.,-0.707106781186547));
#5391=DIRECTION('center_axis',(0.,1.,0.));
#5392=DIRECTION('ref_axis',(-0.707106781186548,0.,-0.707106781186547));
#6547=CARTESIAN_POINT('',(0.,0.,0.));
#6548=CARTESIAN_POINT('Origin',(0.,-3.,109.33240815703));
#6549=CARTESIAN_POINT('',(0.,-3.,109.33240815703));
#6550=CARTESIAN_POINT('',(0.,-3.,80.5324081570305));
#6551=CARTESIAN_POINT('',(0.,-3.,111.83240815703));
#6552=CARTESIAN_POINT('',(0.,-2.9,109.33240815703));
#6553=CARTESIAN_POINT('',(0.,-3.,109.33240815703));
#6554=CARTESIAN_POINT('',(0.,-2.9,80.5324081570305));
#6555=CARTESIAN_POINT('',(0.,-2.9,111.83240815703));
#6556=CARTESIAN_POINT('',(0.,-3.,80.5324081570305));
#6557=CARTESIAN_POINT('Origin',(23.9002092041053,-3.,90.4321989529251));
#6558=CARTESIAN_POINT('',(23.9002092041053,-3.,90.4321989529251));
#6559=CARTESIAN_POINT('',(3.53553390593275,-3.,110.796874251098));
#6560=CARTESIAN_POINT('',(11.9501046020527,-3.,102.382303554978));
#6561=CARTESIAN_POINT('',(23.9002092041053,-2.9,90.4321989529251));
#6562=CARTESIAN_POINT('',(23.9002092041053,-3.,90.4321989529251));
#6563=CARTESIAN_POINT('',(3.53553390593275,-2.9,110.796874251098));
#6564=CARTESIAN_POINT('',(11.9501046020527,-2.9,102.382303554978));
#6565=CARTESIAN_POINT('',(3.53553390593275,-3.,110.796874251098));
#6566=CARTESIAN_POINT('Origin',(0.,-3.,114.33240815703));
#6567=CARTESIAN_POINT('Origin',(0.,-3.,114.33240815703));
#6568=CARTESIAN_POINT('Origin',(0.,-3.,114.33240815703));
#6569=CARTESIAN_POINT('',(16.5043001764605,-3.,90.4679504876131));
#6570=CARTESIAN_POINT('Origin',(15.7264827171553,-3.,89.6901330283079));
#6571=CARTESIAN_POINT('',(5.87700253253308,-3.,86.3254676051657));
#6572=CARTESIAN_POINT('Origin',(5.09918507322787,-3.,85.5476501458605));
#6573=CARTESIAN_POINT('Origin',(15.7264827171553,-3.,89.6901330283079));
#6574=CARTESIAN_POINT('',(16.5043001764605,-3.5,90.4679504876131));
#6575=CARTESIAN_POINT('Origin',(15.7264827171553,-3.5,89.6901330283079));
#6576=CARTESIAN_POINT('',(16.5043001764605,-3.,90.4679504876131));
#6577=CARTESIAN_POINT('Origin',(15.7264827171553,-3.5,89.6901330283079));
#6578=CARTESIAN_POINT('Origin',(5.09918507322787,-3.,85.5476501458605));
#6579=CARTESIAN_POINT('',(5.87700253253308,-3.5,86.3254676051657));
#6580=CARTESIAN_POINT('Origin',(5.09918507322787,-3.5,85.5476501458605));
#6581=CARTESIAN_POINT('',(5.87700253253308,-3.,86.3254676051657));
#6582=CARTESIAN_POINT('Origin',(5.09918507322787,-3.5,85.5476501458605));
#6583=CARTESIAN_POINT('Origin',(0.,-3.,114.33240815703));
#6584=CARTESIAN_POINT('Origin',(0.,-2.9,114.33240815703));
#6585=CARTESIAN_POINT('Origin',(0.,-3.,114.33240815703));
#6586=CARTESIAN_POINT('Origin',(0.,-2.9,114.33240815703));
#6587=CARTESIAN_POINT('Origin',(0.,-2.9,114.33240815703));
#6734=UNCERTAINTY_MEASURE_WITH_UNIT(LENGTH_MEASURE(0.01),#6754,
'DISTANCE_ACCURACY_VALUE',
'Maximum model space distance between geometric entities at asserted c
onnectivities');
#6738=UNCERTAINTY_MEASURE_WITH_UNIT(LENGTH_MEASURE(0.01),#6754,
'DISTANCE_ACCURACY_VALUE',
'Maximum model space distance between geometric entities at asserted c
onnectivities');
#6749=(
GEOMETRIC_REPRESENTATION_CONTEXT(3)
GLOBAL_UNCERTAINTY_ASSIGNED_CONTEXT((#6734))
GLOBAL_UNIT_ASSIGNED_CONTEXT((#6754,#6756,#6757))
REPRESENTATION_CONTEXT('','3D')
);
#6753=(
GEOMETRIC_REPRESENTATION_CONTEXT(3)
GLOBAL_UNCERTAINTY_ASSIGNED_CONTEXT((#6738))
GLOBAL_UNIT_ASSIGNED_CONTEXT((#6754,#6756,#6757))
REPRESENTATION_CONTEXT('','3D')
);
#6754=(
LENGTH_UNIT()
NAMED_UNIT(*)
SI_UNIT(.MILLI.,.METRE.)
);
#6756=(
NAMED_UNIT(*)
PLANE_ANGLE_UNIT()
SI_UNIT($,.RADIAN.)
);
#6757=(
NAMED_UNIT(*)
SI_UNIT($,.STERADIAN.)
SOLID_ANGLE_UNIT()
);
#6768=SHAPE_DEFINITION_REPRESENTATION(#6782,#6809);
#6782=PRODUCT_DEFINITION_SHAPE('',$,#6824);
#6809=SHAPE_REPRESENTATION('',(#4276),#6749);
#6813=PRODUCT_DEFINITION_CONTEXT('part definition',#6857,'design');
#6824=PRODUCT_DEFINITION('Blade_06','Blade_06',#6838,#6813);
#6838=PRODUCT_DEFINITION_FORMATION('',$,#6869);
#6857=APPLICATION_CONTEXT(
'Core Data for Automotive Mechanical Design Process');
#6858=PRODUCT_CONTEXT('part definition',#6857,'mechanical');
#6869=PRODUCT('Blade_06','Blade_06',$,(#6858));
#6929=COLOUR_RGB('Off White',0.89,0.88,0.83);
#6930=FILL_AREA_STYLE_COLOUR('',#6929);
#6931=FILL_AREA_STYLE('',(#6930));
#6932=SURFACE_STYLE_FILL_AREA(#6931);
#6933=SURFACE_SIDE_STYLE('',(#6932));
#6934=SURFACE_STYLE_USAGE(.BOTH.,#6933);
#6935=PRESENTATION_STYLE_ASSIGNMENT((#6934));
ENDSEC;
END-ISO-10303-21;
